ISO-10303-21;
HEADER;
FILE_DESCRIPTION (('STEP AP214'),
    '1' );
FILE_NAME ('socket head cap screw_iso_ISO 4762 M4 x 20 - 20N.step',
    '2026-10-08T12:12:07',
    ( '' ),
    ( '' ),
    'SwSTEP 2.0',
    'SolidWorks 2026',
    '' );
FILE_SCHEMA (( 'AUTOMOTIVE_DESIGN' ));
ENDSEC;

DATA;
#4=ORIENTED_EDGE ( 'NONE', *, *, #3995, .T. ) ;
#11=CIRCLE ( 'NONE', #4655, 3.299999999999999822 ) ;
#15=ORIENTED_EDGE ( 'NONE', *, *, #6393, .F. ) ;
#32=EDGE_LOOP ( 'NONE', ( #2251, #1109, #2656, #3323 ) ) ;
#45=DIRECTION ( 'NONE',  ( 1.000000000000000000, 0.000000000000000000, 0.000000000000000000 ) ) ;
#48=EDGE_CURVE ( 'NONE', #4570, #1158, #4656, .T. ) ;
#56=DIRECTION ( 'NONE',  ( 0.000000000000000000, 0.000000000000000000, 1.000000000000000000 ) ) ;
#65=EDGE_LOOP ( 'NONE', ( #3334, #6750, #4812, #6687 ) ) ;
#76=EDGE_LOOP ( 'NONE', ( #7963, #1978, #1867, #3396 ) ) ;
#85=ORIENTED_EDGE ( 'NONE', *, *, #3347, .T. ) ;
#100=EDGE_CURVE ( 'NONE', #953, #6924, #7257, .T. ) ;
#106=ORIENTED_EDGE ( 'NONE', *, *, #2494, .F. ) ;
#112=CONICAL_SURFACE ( 'NONE', #2379, 1.535500000000000087, 1.047197551196590748 ) ;
#122=EDGE_LOOP ( 'NONE', ( #168, #7429, #374, #2887 ) ) ;
#124=VECTOR ( 'NONE', #3649, 1000.000000000000000 ) ;
#135=VERTEX_POINT ( 'NONE', #2859 ) ;
#136=AXIS2_PLACEMENT_3D ( 'NONE', #1715, #4290, #4376 ) ;
#139=DIRECTION ( 'NONE',  ( 0.000000000000000000, 0.000000000000000000, 1.000000000000000000 ) ) ;
#151=DIRECTION ( 'NONE',  ( 0.000000000000000000, 0.000000000000000000, 1.000000000000000000 ) ) ;
#161=AXIS2_PLACEMENT_3D ( 'NONE', #5599, #2306, #1096 ) ;
#168=ORIENTED_EDGE ( 'NONE', *, *, #3674, .T. ) ;
#172=DIRECTION ( 'NONE',  ( -0.000000000000000000, 1.000000000000000000, 1.224646799147353207E-16 ) ) ;
#174=EDGE_CURVE ( 'NONE', #7038, #1738, #1989, .T. ) ;
#197=EDGE_CURVE ( 'NONE', #2405, #1419, #5179, .T. ) ;
#263=CARTESIAN_POINT ( 'NONE',  ( 0.000000000000000000, 0.000000000000000000, 0.000000000000000000 ) ) ;
#281=VECTOR ( 'NONE', #2931, 1000.000000000000000 ) ;
#291=EDGE_CURVE ( 'NONE', #5142, #1419, #574, .T. ) ;
#312=DIRECTION ( 'NONE',  ( 0.000000000000000000, 0.000000000000000000, 1.000000000000000000 ) ) ;
#321=ORIENTED_EDGE ( 'NONE', *, *, #7755, .T. ) ;
#325=EDGE_CURVE ( 'NONE', #2405, #6988, #1374, .T. ) ;
#327=CARTESIAN_POINT ( 'NONE',  ( 2.000000000000000000, -0.8865213383406690406, 1.535500000000000975 ) ) ;
#341=CARTESIAN_POINT ( 'NONE',  ( 2.000000000000000000, 1.773042676681340968, -2.276824562219559311E-15 ) ) ;
#360=DIRECTION ( 'NONE',  ( -0.000000000000000000, 1.467581828789149729E-15, 1.000000000000000000 ) ) ;
#374=ORIENTED_EDGE ( 'NONE', *, *, #6408, .F. ) ;
#386=EDGE_CURVE ( 'NONE', #1419, #3458, #8149, .T. ) ;
#390=FACE_OUTER_BOUND ( 'NONE', #5670, .T. ) ;
#410=ORIENTED_EDGE ( 'NONE', *, *, #5702, .T. ) ;
#416=( NAMED_UNIT ( * ) PLANE_ANGLE_UNIT ( ) SI_UNIT ( $, .RADIAN. ) );
#438=ADVANCED_FACE ( 'NONE', ( #5350 ), #3256, .T. ) ;
#448=PLANE ( 'NONE',  #1317 ) ;
#455=CARTESIAN_POINT ( 'NONE',  ( 0.1999999999999987899, 0.000000000000000000, 0.000000000000000000 ) ) ;
#460=SURFACE_STYLE_FILL_AREA ( #2508 ) ;
#465=ORIENTED_EDGE ( 'NONE', *, *, #6394, .T. ) ;
#478=FACE_OUTER_BOUND ( 'NONE', #6860, .T. ) ;
#491=VECTOR ( 'NONE', #6667, 1000.000000000000000 ) ;
#498=PRESENTATION_STYLE_ASSIGNMENT (( #2994 ) ) ;
#520=DIRECTION ( 'NONE',  ( 0.000000000000000000, 0.000000000000000000, 1.000000000000000000 ) ) ;
#523=FACE_OUTER_BOUND ( 'NONE', #5652, .T. ) ;
#526=AXIS2_PLACEMENT_3D ( 'NONE', #6005, #4849, #7374 ) ;
#531=VERTEX_POINT ( 'NONE', #7902 ) ;
#538=LINE ( 'NONE', #3874, #5170 ) ;
#541=ORIENTED_EDGE ( 'NONE', *, *, #8079, .F. ) ;
#547=FACE_OUTER_BOUND ( 'NONE', #4009, .T. ) ;
#558=PLANE ( 'NONE',  #3293 ) ;
#560=FILL_AREA_STYLE ('',( #1138 ) ) ;
#569=CARTESIAN_POINT ( 'NONE',  ( 0.000000000000000000, 1.773042676681340968, -2.276824562219559311E-15 ) ) ;
#574=LINE ( 'NONE', #7718, #7494 ) ;
#587=CARTESIAN_POINT ( 'NONE',  ( 0.000000000000000000, 0.8865213383406685965, -1.535500000000000753 ) ) ;
#594=ADVANCED_FACE ( 'NONE', ( #2269 ), #7951, .F. ) ;
#606=CARTESIAN_POINT ( 'NONE',  ( 2.000000000000000000, -0.8865213383406690406, 1.535500000000000975 ) ) ;
#612=CARTESIAN_POINT ( 'NONE',  ( 2.000000000000000000, 1.773042676681340968, -2.276824562219559311E-15 ) ) ;
#635=ORIENTED_EDGE ( 'NONE', *, *, #1241, .F. ) ;
#636=AXIS2_PLACEMENT_3D ( 'NONE', #4081, #799, #139 ) ;
#641=DIRECTION ( 'NONE',  ( -1.000000000000000000, -0.000000000000000000, -0.000000000000000000 ) ) ;
#669=EDGE_CURVE ( 'NONE', #6853, #3935, #3755, .T. ) ;
#672=DIRECTION ( 'NONE',  ( 0.000000000000000000, 0.4999999999999990008, -0.8660254037844391517 ) ) ;
#687=EDGE_CURVE ( 'NONE', #3935, #4267, #2668, .T. ) ;
#694=VECTOR ( 'NONE', #4778, 1000.000000000000114 ) ;
#695=EDGE_LOOP ( 'NONE', ( #85, #6665, #2157, #3298, #410 ) ) ;
#704=EDGE_LOOP ( 'NONE', ( #7531, #5984, #1710, #635 ) ) ;
#711=LINE ( 'NONE', #1935, #3202 ) ;
#731=DIRECTION ( 'NONE',  ( -1.000000000000000000, -0.000000000000000000, -0.000000000000000000 ) ) ;
#761=CARTESIAN_POINT ( 'NONE',  ( 0.000000000000000000, -1.773042676681340968, 2.059984127722458425E-15 ) ) ;
#770=CIRCLE ( 'NONE', #7805, 3.500000000000000000 ) ;
#773=AXIS2_PLACEMENT_3D ( 'NONE', #3782, #8203, #7599 ) ;
#784=EDGE_CURVE ( 'NONE', #5142, #2405, #1146, .T. ) ;
#799=DIRECTION ( 'NONE',  ( -1.000000000000000000, -0.000000000000000000, -0.000000000000000000 ) ) ;
#800=AXIS2_PLACEMENT_3D ( 'NONE', #6568, #4091, #5882 ) ;
#801=EDGE_CURVE ( 'NONE', #1617, #2702, #1330, .T. ) ;
#821=VERTEX_POINT ( 'NONE', #569 ) ;
#843=AXIS2_PLACEMENT_3D ( 'NONE', #341, #6666, #5431 ) ;
#890=DIRECTION ( 'NONE',  ( 0.000000000000000000, 0.000000000000000000, -1.000000000000000000 ) ) ;
#898=AXIS2_PLACEMENT_3D ( 'NONE', #2358, #4407, #3160 ) ;
#903=FACE_OUTER_BOUND ( 'NONE', #5048, .T. ) ;
#904=EDGE_CURVE ( 'NONE', #5852, #7486, #7424, .T. ) ;
#912=TOROIDAL_SURFACE ( 'NONE', #5306, 3.299999999999999822, 0.2000000000000000111 ) ;
#946=CARTESIAN_POINT ( 'NONE',  ( 0.000000000000000000, 0.000000000000000000, 0.000000000000000000 ) ) ;
#948=AXIS2_PLACEMENT_3D ( 'NONE', #4184, #2277, #6673 ) ;
#953=VERTEX_POINT ( 'NONE', #761 ) ;
#960=DIRECTION ( 'NONE',  ( -1.000000000000000000, -0.000000000000000000, -0.000000000000000000 ) ) ;
#994=EDGE_LOOP ( 'NONE', ( #6655, #4917, #4187, #7876, #6236 ) ) ;
#1013=ORIENTED_EDGE ( 'NONE', *, *, #3541, .T. ) ;
#1014=PLANE ( 'NONE',  #3687 ) ;
#1024=CIRCLE ( 'NONE', #636, 2.000000000000000444 ) ;
#1026=DIRECTION ( 'NONE',  ( 0.000000000000000000, 0.000000000000000000, 1.000000000000000000 ) ) ;
#1040=CARTESIAN_POINT ( 'NONE',  ( 2.000000000000000000, 1.773042676681340968, -2.276824562219559311E-15 ) ) ;
#1042=AXIS2_PLACEMENT_3D ( 'NONE', #8002, #5404, #6140 ) ;
#1045=VECTOR ( 'NONE', #4892, 1000.000000000000000 ) ;
#1062=CARTESIAN_POINT ( 'NONE',  ( 2.000000000000000000, -1.773042676681340968, 2.059984127722458425E-15 ) ) ;
#1066=COLOUR_RGB ( '', 0.09019608, 0.27058824, 0.51372549) ;
#1067=DIRECTION ( 'NONE',  ( 0.000000000000000000, 1.224646799147353207E-16, 1.000000000000000000 ) ) ;
#1077=FACE_OUTER_BOUND ( 'NONE', #695, .T. ) ;
#1084=DIRECTION ( 'NONE',  ( -1.000000000000000000, -0.000000000000000000, -0.000000000000000000 ) ) ;
#1096=DIRECTION ( 'NONE',  ( 0.000000000000000000, 0.000000000000000000, 1.000000000000000000 ) ) ;
#1109=ORIENTED_EDGE ( 'NONE', *, *, #3372, .T. ) ;
#1117=EDGE_CURVE ( 'NONE', #2702, #6185, #2402, .T. ) ;
#1119=VECTOR ( 'NONE', #2487, 1000.000000000000114 ) ;
#1129=( NAMED_UNIT ( * ) SI_UNIT ( $, .STERADIAN. ) SOLID_ANGLE_UNIT ( ) );
#1138=FILL_AREA_STYLE_COLOUR ( '', #1066 ) ;
#1146=LINE ( 'NONE', #3686, #2655 ) ;
#1158=VERTEX_POINT ( 'NONE', #5957 ) ;
#1176=CIRCLE ( 'NONE', #1042, 2.000000000000000444 ) ;
#1183=( LENGTH_UNIT ( ) NAMED_UNIT ( * ) SI_UNIT ( .MILLI., .METRE. ) );
#1195=PLANE ( 'NONE',  #773 ) ;
#1202=VECTOR ( 'NONE', #1084, 1000.000000000000000 ) ;
#1237=DIRECTION ( 'NONE',  ( -1.000000000000000000, -0.000000000000000000, -0.000000000000000000 ) ) ;
#1241=EDGE_CURVE ( 'NONE', #531, #3462, #11, .T. ) ;
#1247=MANIFOLD_SOLID_BREP ( 'Hex', #5947 ) ;
#1253=MECHANICAL_DESIGN_GEOMETRIC_PRESENTATION_REPRESENTATION('',(#7490),#5889);
#1269=DIRECTION ( 'NONE',  ( 0.000000000000000000, 0.000000000000000000, 1.000000000000000000 ) ) ;
#1298=EDGE_CURVE ( 'NONE', #3935, #7038, #4529, .T. ) ;
#1299=ORIENTED_EDGE ( 'NONE', *, *, #6393, .T. ) ;
#1301=FACE_OUTER_BOUND ( 'NONE', #5738, .T. ) ;
#1312=AXIS2_PLACEMENT_3D ( 'NONE', #4807, #4847, #7334 ) ;
#1317=AXIS2_PLACEMENT_3D ( 'NONE', #8097, #360, #4859 ) ;
#1330=CIRCLE ( 'NONE', #2383, 0.2000000000000000944 ) ;
#1334=AXIS2_PLACEMENT_3D ( 'NONE', #7590, #3855, #1397 ) ;
#1374=LINE ( 'NONE', #612, #1119 ) ;
#1384=ORIENTED_EDGE ( 'NONE', *, *, #1760, .T. ) ;
#1397=DIRECTION ( 'NONE',  ( 0.000000000000000000, 0.000000000000000000, 1.000000000000000000 ) ) ;
#1408=CARTESIAN_POINT ( 'NONE',  ( 2.000000000000000000, 0.000000000000000000, 0.000000000000000000 ) ) ;
#1419=VERTEX_POINT ( 'NONE', #5911 ) ;
#1433=LINE ( 'NONE', #6562, #6338 ) ;
#1459=ORIENTED_EDGE ( 'NONE', *, *, #8079, .T. ) ;
#1460=CIRCLE ( 'NONE', #2781, 2.200000000000001066 ) ;
#1496=UNCERTAINTY_MEASURE_WITH_UNIT (LENGTH_MEASURE( 1.000000000000000082E-05 ), #1674, 'distance_accuracy_value', 'NONE');
#1499=CARTESIAN_POINT ( 'NONE',  ( 0.000000000000000000, -1.773042676681340968, 2.059984127722458425E-15 ) ) ;
#1514=LINE ( 'NONE', #2716, #2239 ) ;
#1520=ORIENTED_EDGE ( 'NONE', *, *, #669, .F. ) ;
#1531=CYLINDRICAL_SURFACE ( 'NONE', #5398, 3.500000000000000000 ) ;
#1578=DIRECTION ( 'NONE',  ( -1.000000000000000000, -0.000000000000000000, -0.000000000000000000 ) ) ;
#1587=AXIS2_PLACEMENT_3D ( 'NONE', #3942, #5152, #6454 ) ;
#1617=VERTEX_POINT ( 'NONE', #7791 ) ;
#1659=ORIENTED_EDGE ( 'NONE', *, *, #3995, .F. ) ;
#1670=ORIENTED_EDGE ( 'NONE', *, *, #3650, .T. ) ;
#1674=( LENGTH_UNIT ( ) NAMED_UNIT ( * ) SI_UNIT ( .MILLI., .METRE. ) );
#1675=ADVANCED_FACE ( 'NONE', ( #3953 ), #1531, .T. ) ;
#1678=VERTEX_POINT ( 'NONE', #2154 ) ;
#1697=DIRECTION ( 'NONE',  ( -1.000000000000000000, -0.000000000000000000, -0.000000000000000000 ) ) ;
#1699=ORIENTED_EDGE ( 'NONE', *, *, #1760, .F. ) ;
#1708=CIRCLE ( 'NONE', #1312, 2.000000000000000888 ) ;
#1710=ORIENTED_EDGE ( 'NONE', *, *, #2840, .T. ) ;
#1713=PLANE ( 'NONE',  #3048 ) ;
#1715=CARTESIAN_POINT ( 'NONE',  ( 4.199999999999995737, 0.000000000000000000, 0.000000000000000000 ) ) ;
#1722=EDGE_CURVE ( 'NONE', #7485, #3458, #4689, .T. ) ;
#1734=PRESENTATION_STYLE_ASSIGNMENT (( #6788 ) ) ;
#1738=VERTEX_POINT ( 'NONE', #7216 ) ;
#1746=CARTESIAN_POINT ( 'NONE',  ( 4.199999999999995737, 2.694222958124178486E-16, 2.200000000000001066 ) ) ;
#1757=ORIENTED_EDGE ( 'NONE', *, *, #1805, .F. ) ;
#1758=ORIENTED_EDGE ( 'NONE', *, *, #3166, .T. ) ;
#1760=EDGE_CURVE ( 'NONE', #3458, #3935, #6566, .T. ) ;
#1789=CARTESIAN_POINT ( 'NONE',  ( 2.000000000000000000, 0.000000000000000000, 0.000000000000000000 ) ) ;
#1794=DIRECTION ( 'NONE',  ( 0.000000000000000000, -0.5000000000000008882, -0.8660254037844380415 ) ) ;
#1805=EDGE_CURVE ( 'NONE', #7038, #6853, #6010, .T. ) ;
#1816=( NAMED_UNIT ( * ) PLANE_ANGLE_UNIT ( ) SI_UNIT ( $, .RADIAN. ) );
#1831=LINE ( 'NONE', #2451, #7552 ) ;
#1838=EDGE_LOOP ( 'NONE', ( #7912, #4288, #1384, #3235, #6147 ) ) ;
#1857=VECTOR ( 'NONE', #3657, 1000.000000000000000 ) ;
#1867=ORIENTED_EDGE ( 'NONE', *, *, #5059, .T. ) ;
#1878=TOROIDAL_SURFACE ( 'NONE', #136, 2.200000000000001066, 0.2000000000000000111 ) ;
#1921=CARTESIAN_POINT ( 'NONE',  ( 24.00000000000000000, 1.971681346627238735E-16, -1.610000000000000098 ) ) ;
#1924=EDGE_CURVE ( 'NONE', #6853, #953, #3157, .T. ) ;
#1929=EDGE_LOOP ( 'NONE', ( #1659, #1013, #4295 ) ) ;
#1935=CARTESIAN_POINT ( 'NONE',  ( 2.000000000000000000, 0.000000000000000000, 1.535500000000000087 ) ) ;
#1953=ADVANCED_FACE ( 'NONE', ( #478 ), #6050, .F. ) ;
#1978=ORIENTED_EDGE ( 'NONE', *, *, #2262, .T. ) ;
#1987=AXIS2_PLACEMENT_3D ( 'NONE', #946, #4279, #1026 ) ;
#1989=CIRCLE ( 'NONE', #3035, 1.535500000000000087 ) ;
#2008=CARTESIAN_POINT ( 'NONE',  ( 24.00000000000000000, 2.210487472460972698E-16, -1.610000000000000098 ) ) ;
#2041=CARTESIAN_POINT ( 'NONE',  ( 4.000000000000003553, 0.000000000000000000, 3.500000000000000000 ) ) ;
#2047=CARTESIAN_POINT ( 'NONE',  ( 2.000000000000000000, -1.773042676681340968, 2.059984127722458425E-15 ) ) ;
#2055=ORIENTED_EDGE ( 'NONE', *, *, #1805, .T. ) ;
#2091=CARTESIAN_POINT ( 'NONE',  ( 2.000000000000000000, 1.773042676681340968, -2.276824562219559311E-15 ) ) ;
#2099=CARTESIAN_POINT ( 'NONE',  ( 0.000000000000000000, -0.8865213383406721492, -1.535499999999999199 ) ) ;
#2114=DIRECTION ( 'NONE',  ( 0.000000000000000000, 0.000000000000000000, -1.000000000000000000 ) ) ;
#2130=EDGE_LOOP ( 'NONE', ( #2469, #3665, #7353, #7621 ) ) ;
#2134=STYLED_ITEM ( 'NONE', ( #1734 ), #1247 ) ;
#2143=ORIENTED_EDGE ( 'NONE', *, *, #197, .F. ) ;
#2154=CARTESIAN_POINT ( 'NONE',  ( 2.000000000000000000, -0.8865213383406690406, 1.535500000000000975 ) ) ;
#2157=ORIENTED_EDGE ( 'NONE', *, *, #8069, .F. ) ;
#2208=LINE ( 'NONE', #4872, #4781 ) ;
#2229=FACE_OUTER_BOUND ( 'NONE', #76, .T. ) ;
#2239=VECTOR ( 'NONE', #7777, 1000.000000000000000 ) ;
#2240=DIRECTION ( 'NONE',  ( -1.000000000000000000, -0.000000000000000000, -0.000000000000000000 ) ) ;
#2251=ORIENTED_EDGE ( 'NONE', *, *, #4713, .F. ) ;
#2254=DIRECTION ( 'NONE',  ( 0.000000000000000000, -1.224646799147353207E-16, 1.000000000000000000 ) ) ;
#2262=EDGE_CURVE ( 'NONE', #4453, #7189, #2968, .T. ) ;
#2269=FACE_OUTER_BOUND ( 'NONE', #7338, .T. ) ;
#2276=ADVANCED_FACE ( 'NONE', ( #5474 ), #3601, .T. ) ;
#2277=DIRECTION ( 'NONE',  ( -1.000000000000000000, -0.000000000000000000, -0.000000000000000000 ) ) ;
#2296=PLANE ( 'NONE',  #7161 ) ;
#2306=DIRECTION ( 'NONE',  ( -1.000000000000000000, -0.000000000000000000, -0.000000000000000000 ) ) ;
#2331=FACE_OUTER_BOUND ( 'NONE', #5180, .T. ) ;
#2337=ORIENTED_EDGE ( 'NONE', *, *, #3674, .F. ) ;
#2345=EDGE_LOOP ( 'NONE', ( #7725, #3083, #465, #2855 ) ) ;
#2358=CARTESIAN_POINT ( 'NONE',  ( -31.74999999999995737, 0.000000000000000000, 0.000000000000000000 ) ) ;
#2365=ADVANCED_FACE ( 'NONE', ( #2229 ), #2728, .T. ) ;
#2367=APPLICATION_CONTEXT ( 'automotive_design' ) ;
#2368=VECTOR ( 'NONE', #2240, 1000.000000000000000 ) ;
#2374=DIRECTION ( 'NONE',  ( 0.000000000000000000, -0.4999999999999990563, 0.8660254037844391517 ) ) ;
#2379=AXIS2_PLACEMENT_3D ( 'NONE', #6250, #4972, #2926 ) ;
#2383=AXIS2_PLACEMENT_3D ( 'NONE', #1746, #6884, #1067 ) ;
#2400=DIRECTION ( 'NONE',  ( 0.000000000000000000, 0.000000000000000000, 1.000000000000000000 ) ) ;
#2402=CIRCLE ( 'NONE', #800, 2.200000000000001066 ) ;
#2405=VERTEX_POINT ( 'NONE', #7302 ) ;
#2413=ADVANCED_FACE ( 'NONE', ( #5276 ), #7337, .T. ) ;
#2415=LINE ( 'NONE', #5089, #5290 ) ;
#2419=AXIS2_PLACEMENT_3D ( 'NONE', #6581, #4105, #2114 ) ;
#2449=DIRECTION ( 'NONE',  ( -1.000000000000000000, -0.000000000000000000, -0.000000000000000000 ) ) ;
#2451=CARTESIAN_POINT ( 'NONE',  ( 0.000000000000000000, 1.773042676681340968, -2.276824562219559311E-15 ) ) ;
#2455=AXIS2_PLACEMENT_3D ( 'NONE', #7243, #2848, #151 ) ;
#2460=ORIENTED_EDGE ( 'NONE', *, *, #784, .T. ) ;
#2465=SURFACE_SIDE_STYLE ('',( #460 ) ) ;
#2469=ORIENTED_EDGE ( 'NONE', *, *, #6408, .T. ) ;
#2487=DIRECTION ( 'NONE',  ( 0.000000000000000000, -0.4999999999999993339, 0.8660254037844389297 ) ) ;
#2488=CARTESIAN_POINT ( 'NONE',  ( 2.000000000000000000, 0.8865213383406685965, -1.535500000000000753 ) ) ;
#2494=EDGE_CURVE ( 'NONE', #821, #7449, #5439, .T. ) ;
#2508=FILL_AREA_STYLE ('',( #5502 ) ) ;
#2550=EDGE_LOOP ( 'NONE', ( #3124, #4296 ) ) ;
#2582=DIRECTION ( 'NONE',  ( -1.000000000000000000, -0.000000000000000000, -0.000000000000000000 ) ) ;
#2597=DIRECTION ( 'NONE',  ( 0.000000000000000000, 0.000000000000000000, -1.000000000000000000 ) ) ;
#2628=CARTESIAN_POINT ( 'NONE',  ( 2.000000000000000000, 1.773042676681340968, -2.276824562219559311E-15 ) ) ;
#2636=PLANE ( 'NONE',  #6488 ) ;
#2646=AXIS2_PLACEMENT_3D ( 'NONE', #4950, #2449, #3616 ) ;
#2655=VECTOR ( 'NONE', #6758, 1000.000000000000114 ) ;
#2656=ORIENTED_EDGE ( 'NONE', *, *, #2929, .T. ) ;
#2667=ORIENTED_EDGE ( 'NONE', *, *, #3459, .T. ) ;
#2668=LINE ( 'NONE', #3839, #7939 ) ;
#2691=ORIENTED_EDGE ( 'NONE', *, *, #5402, .F. ) ;
#2702=VERTEX_POINT ( 'NONE', #4953 ) ;
#2704=CARTESIAN_POINT ( 'NONE',  ( 2.000000000000000000, 0.8865213383406685965, -1.535500000000000753 ) ) ;
#2705=DIRECTION ( 'NONE',  ( 0.000000000000000000, 0.000000000000000000, -1.000000000000000000 ) ) ;
#2707=CARTESIAN_POINT ( 'NONE',  ( 2.000000000000000000, 0.8865213383406685965, -1.535500000000000753 ) ) ;
#2713=CARTESIAN_POINT ( 'NONE',  ( 24.00000000000000000, 0.000000000000000000, 1.610000000000000098 ) ) ;
#2716=CARTESIAN_POINT ( 'NONE',  ( -31.74999999999995737, 2.449293598294707893E-16, -2.000000000000000888 ) ) ;
#2723=DIRECTION ( 'NONE',  ( 0.000000000000000000, 0.5000000000000011102, 0.8660254037844379305 ) ) ;
#2728=CYLINDRICAL_SURFACE ( 'NONE', #948, 3.500000000000000000 ) ;
#2732=UNCERTAINTY_MEASURE_WITH_UNIT (LENGTH_MEASURE( 1.000000000000000082E-05 ), #7276, 'distance_accuracy_value', 'NONE');
#2738=VECTOR ( 'NONE', #1697, 1000.000000000000000 ) ;
#2754=CIRCLE ( 'NONE', #7774, 0.2000000000000000944 ) ;
#2773=VECTOR ( 'NONE', #6170, 1000.000000000000000 ) ;
#2780=ADVANCED_FACE ( 'NONE', ( #5529 ), #8043, .T. ) ;
#2781=AXIS2_PLACEMENT_3D ( 'NONE', #4338, #4389, #8068 ) ;
#2796=APPLICATION_CONTEXT ( 'automotive_design' ) ;
#2840=EDGE_CURVE ( 'NONE', #7486, #3462, #2754, .T. ) ;
#2848=DIRECTION ( 'NONE',  ( -1.000000000000000000, -0.000000000000000000, -0.000000000000000000 ) ) ;
#2855=ORIENTED_EDGE ( 'NONE', *, *, #3372, .F. ) ;
#2856=DIRECTION ( 'NONE',  ( -1.000000000000000000, -0.000000000000000000, -0.000000000000000000 ) ) ;
#2859=CARTESIAN_POINT ( 'NONE',  ( 0.000000000000000000, -0.8865213383406690406, 1.535500000000000975 ) ) ;
#2872=DIRECTION ( 'NONE',  ( 0.000000000000000000, 1.000000000000000000, -1.467581828789149532E-15 ) ) ;
#2881=UNCERTAINTY_MEASURE_WITH_UNIT (LENGTH_MEASURE( 1.000000000000000082E-05 ), #1183, 'distance_accuracy_value', 'NONE');
#2885=AXIS2_PLACEMENT_3D ( 'NONE', #6211, #1237, #6833 ) ;
#2887=ORIENTED_EDGE ( 'NONE', *, *, #6394, .F. ) ;
#2916=DIRECTION ( 'NONE',  ( -1.000000000000000000, -0.000000000000000000, -0.000000000000000000 ) ) ;
#2917=CARTESIAN_POINT ( 'NONE',  ( 2.000000000000000000, -0.8865213383406721492, -1.535499999999999199 ) ) ;
#2926=DIRECTION ( 'NONE',  ( 0.000000000000000000, 0.000000000000000000, 1.000000000000000000 ) ) ;
#2929=EDGE_CURVE ( 'NONE', #4177, #1617, #3949, .T. ) ;
#2931=DIRECTION ( 'NONE',  ( -1.000000000000000000, -0.000000000000000000, -0.000000000000000000 ) ) ;
#2943=EDGE_LOOP ( 'NONE', ( #2337, #7091 ) ) ;
#2954=ORIENTED_EDGE ( 'NONE', *, *, #8069, .T. ) ;
#2968=LINE ( 'NONE', #5514, #281 ) ;
#2982=FACE_OUTER_BOUND ( 'NONE', #32, .T. ) ;
#2991=CARTESIAN_POINT ( 'NONE',  ( 2.886521338340684917, 0.000000000000000000, 0.000000000000000000 ) ) ;
#2994=SURFACE_STYLE_USAGE ( .BOTH. , #2465 ) ;
#3028=ORIENTED_EDGE ( 'NONE', *, *, #801, .T. ) ;
#3035=AXIS2_PLACEMENT_3D ( 'NONE', #1789, #4903, #6889 ) ;
#3048=AXIS2_PLACEMENT_3D ( 'NONE', #8014, #4249, #2374 ) ;
#3083=ORIENTED_EDGE ( 'NONE', *, *, #8017, .T. ) ;
#3097=CARTESIAN_POINT ( 'NONE',  ( 2.000000000000000000, 0.8865213383406685965, -1.535500000000000753 ) ) ;
#3099=DIRECTION ( 'NONE',  ( 0.000000000000000000, 0.000000000000000000, 1.000000000000000000 ) ) ;
#3124=ORIENTED_EDGE ( 'NONE', *, *, #6407, .T. ) ;
#3137=ORIENTED_EDGE ( 'NONE', *, *, #291, .F. ) ;
#3138=ORIENTED_EDGE ( 'NONE', *, *, #325, .T. ) ;
#3147=EDGE_CURVE ( 'NONE', #5852, #4453, #6462, .T. ) ;
#3157=LINE ( 'NONE', #4352, #2738 ) ;
#3160=DIRECTION ( 'NONE',  ( 0.000000000000000000, 0.000000000000000000, 1.000000000000000000 ) ) ;
#3166=EDGE_CURVE ( 'NONE', #7486, #7189, #5932, .T. ) ;
#3193=CARTESIAN_POINT ( 'NONE',  ( 2.000000000000000000, 0.000000000000000000, 0.000000000000000000 ) ) ;
#3195=CONICAL_SURFACE ( 'NONE', #1334, 1.535500000000000087, 1.047197551196590748 ) ;
#3202=VECTOR ( 'NONE', #6985, 1000.000000000000000 ) ;
#3208=DIRECTION ( 'NONE',  ( 0.000000000000000000, -0.5000000000000011102, -0.8660254037844379305 ) ) ;
#3230=DIRECTION ( 'NONE',  ( 0.000000000000000000, 0.8660254037844381525, -0.5000000000000009992 ) ) ;
#3235=ORIENTED_EDGE ( 'NONE', *, *, #1298, .T. ) ;
#3256=CONICAL_SURFACE ( 'NONE', #2455, 1.610000000000000098, 0.7853981633974647103 ) ;
#3263=ADVANCED_FACE ( 'NONE', ( #3730 ), #558, .F. ) ;
#3293=AXIS2_PLACEMENT_3D ( 'NONE', #3097, #5639, #8153 ) ;
#3298=ORIENTED_EDGE ( 'NONE', *, *, #3541, .F. ) ;
#3323=ORIENTED_EDGE ( 'NONE', *, *, #6084, .T. ) ;
#3334=ORIENTED_EDGE ( 'NONE', *, *, #5059, .F. ) ;
#3338=DIRECTION ( 'NONE',  ( 1.000000000000000000, 0.000000000000000000, 0.000000000000000000 ) ) ;
#3347=EDGE_CURVE ( 'NONE', #135, #7449, #1433, .T. ) ;
#3348=AXIS2_PLACEMENT_3D ( 'NONE', #4281, #7433, #6806 ) ;
#3372=EDGE_CURVE ( 'NONE', #5731, #4177, #1024, .T. ) ;
#3396=ORIENTED_EDGE ( 'NONE', *, *, #904, .F. ) ;
#3397=DIRECTION ( 'NONE',  ( -0.5000000000000061062, 1.060575238724902601E-16, -0.8660254037844351549 ) ) ;
#3424=CARTESIAN_POINT ( 'NONE',  ( 0.1999999999999987899, 4.286263797015736595E-16, -3.500000000000000000 ) ) ;
#3447=DIRECTION ( 'NONE',  ( -1.000000000000000000, -0.000000000000000000, -0.000000000000000000 ) ) ;
#3458=VERTEX_POINT ( 'NONE', #3590 ) ;
#3459=EDGE_CURVE ( 'NONE', #135, #953, #2208, .T. ) ;
#3462=VERTEX_POINT ( 'NONE', #4739 ) ;
#3481=FACE_OUTER_BOUND ( 'NONE', #2345, .T. ) ;
#3486=ORIENTED_EDGE ( 'NONE', *, *, #1117, .F. ) ;
#3503=ORIENTED_EDGE ( 'NONE', *, *, #1298, .F. ) ;
#3523=CARTESIAN_POINT ( 'NONE',  ( -31.74999999999995737, 0.000000000000000000, 0.000000000000000000 ) ) ;
#3527=LINE ( 'NONE', #7431, #4232 ) ;
#3541=EDGE_CURVE ( 'NONE', #1678, #1738, #8016, .T. ) ;
#3545=FACE_OUTER_BOUND ( 'NONE', #1838, .T. ) ;
#3547=SURFACE_SIDE_STYLE ('',( #7364 ) ) ;
#3554=ORIENTED_EDGE ( 'NONE', *, *, #2262, .F. ) ;
#3585=PRODUCT_DEFINITION_SHAPE ( 'NONE', 'NONE',  #7665 ) ;
#3590=CARTESIAN_POINT ( 'NONE',  ( 2.000000000000000000, -1.502314598737159623E-15, -1.535500000000000087 ) ) ;
#3600=( NAMED_UNIT ( * ) SI_UNIT ( $, .STERADIAN. ) SOLID_ANGLE_UNIT ( ) );
#3601=CYLINDRICAL_SURFACE ( 'NONE', #161, 2.000000000000000888 ) ;
#3605=DIRECTION ( 'NONE',  ( 0.000000000000000000, 0.000000000000000000, -1.000000000000000000 ) ) ;
#3611=DIRECTION ( 'NONE',  ( 0.000000000000000000, 0.000000000000000000, -1.000000000000000000 ) ) ;
#3616=DIRECTION ( 'NONE',  ( 0.000000000000000000, 0.000000000000000000, 1.000000000000000000 ) ) ;
#3637=CARTESIAN_POINT ( 'NONE',  ( 0.000000000000000000, 0.000000000000000000, 0.000000000000000000 ) ) ;
#3649=DIRECTION ( 'NONE',  ( -1.000000000000000000, -0.000000000000000000, -0.000000000000000000 ) ) ;
#3650=EDGE_CURVE ( 'NONE', #1158, #6924, #4330, .T. ) ;
#3654=ORIENTED_EDGE ( 'NONE', *, *, #801, .F. ) ;
#3657=DIRECTION ( 'NONE',  ( -0.7071067811865359154, 8.659560562355074607E-17, -0.7071067811865591191 ) ) ;
#3660=DIRECTION ( 'NONE',  ( 1.000000000000000000, 0.000000000000000000, 0.000000000000000000 ) ) ;
#3665=ORIENTED_EDGE ( 'NONE', *, *, #4713, .T. ) ;
#3674=EDGE_CURVE ( 'NONE', #5083, #5864, #5560, .T. ) ;
#3685=AXIS2_PLACEMENT_3D ( 'NONE', #6420, #6958, #56 ) ;
#3686=CARTESIAN_POINT ( 'NONE',  ( 2.000000000000000000, 1.773042676681340968, -2.276824562219559311E-15 ) ) ;
#3687=AXIS2_PLACEMENT_3D ( 'NONE', #263, #7295, #5352 ) ;
#3688=DIRECTION ( 'NONE',  ( 1.000000000000000000, 0.000000000000000000, 0.000000000000000000 ) ) ;
#3711=DIRECTION ( 'NONE',  ( 0.000000000000000000, -0.5000000000000011102, -0.8660254037844379305 ) ) ;
#3730=FACE_OUTER_BOUND ( 'NONE', #4854, .T. ) ;
#3755=LINE ( 'NONE', #2047, #7283 ) ;
#3782=CARTESIAN_POINT ( 'NONE',  ( 2.000000000000000000, 1.773042676681340968, -2.276824562219559311E-15 ) ) ;
#3802=DIRECTION ( 'NONE',  ( -1.000000000000000000, -0.000000000000000000, -0.000000000000000000 ) ) ;
#3830=DIRECTION ( 'NONE',  ( 0.000000000000000000, -0.5000000000000011102, -0.8660254037844379305 ) ) ;
#3839=CARTESIAN_POINT ( 'NONE',  ( 2.000000000000000000, -1.773042676681340968, 2.059984127722458425E-15 ) ) ;
#3855=DIRECTION ( 'NONE',  ( -1.000000000000000000, -0.000000000000000000, -0.000000000000000000 ) ) ;
#3858=DIRECTION ( 'NONE',  ( 0.000000000000000000, 0.000000000000000000, 1.000000000000000000 ) ) ;
#3860=EDGE_CURVE ( 'NONE', #4570, #3458, #7734, .T. ) ;
#3874=CARTESIAN_POINT ( 'NONE',  ( 2.000000000000000000, -0.8865213383406690406, 1.535500000000000975 ) ) ;
#3892=FACE_OUTER_BOUND ( 'NONE', #5752, .T. ) ;
#3893=FACE_OUTER_BOUND ( 'NONE', #5465, .T. ) ;
#3908=CARTESIAN_POINT ( 'NONE',  ( 2.000000000000000000, 1.773042676681340968, -2.276824562219559311E-15 ) ) ;
#3935=VERTEX_POINT ( 'NONE', #7387 ) ;
#3942=CARTESIAN_POINT ( 'NONE',  ( 0.000000000000000000, 0.000000000000000000, 0.000000000000000000 ) ) ;
#3949=LINE ( 'NONE', #7786, #7118 ) ;
#3952=VERTEX_POINT ( 'NONE', #8045 ) ;
#3953=FACE_OUTER_BOUND ( 'NONE', #7188, .T. ) ;
#3964=ORIENTED_EDGE ( 'NONE', *, *, #687, .F. ) ;
#3983=CIRCLE ( 'NONE', #6888, 3.500000000000000000 ) ;
#3995=EDGE_CURVE ( 'NONE', #1678, #7038, #2415, .T. ) ;
#4004=ADVANCED_FACE ( 'NONE', ( #5128 ), #7480, .F. ) ;
#4009=EDGE_LOOP ( 'NONE', ( #1520, #1757, #3503 ) ) ;
#4057=CARTESIAN_POINT ( 'NONE',  ( 2.000000000000000000, 1.773042676681340968, -2.276824562219559311E-15 ) ) ;
#4063=ORIENTED_EDGE ( 'NONE', *, *, #48, .F. ) ;
#4081=CARTESIAN_POINT ( 'NONE',  ( 23.61000000000001364, 0.000000000000000000, 0.000000000000000000 ) ) ;
#4091=DIRECTION ( 'NONE',  ( -1.000000000000000000, -0.000000000000000000, -0.000000000000000000 ) ) ;
#4096=VECTOR ( 'NONE', #4693, 1000.000000000000227 ) ;
#4100=DIRECTION ( 'NONE',  ( 1.000000000000000000, 0.000000000000000000, 0.000000000000000000 ) ) ;
#4105=DIRECTION ( 'NONE',  ( 1.000000000000000000, 0.000000000000000000, 0.000000000000000000 ) ) ;
#4114=DIRECTION ( 'NONE',  ( 0.000000000000000000, 0.000000000000000000, 1.000000000000000000 ) ) ;
#4124=DIRECTION ( 'NONE',  ( 1.000000000000000000, 0.000000000000000000, 0.000000000000000000 ) ) ;
#4148=ORIENTED_EDGE ( 'NONE', *, *, #6031, .F. ) ;
#4164=CARTESIAN_POINT ( 'NONE',  ( 0.000000000000000000, 0.8865213383406717051, 1.535499999999998533 ) ) ;
#4168=EDGE_CURVE ( 'NONE', #3952, #1617, #6101, .T. ) ;
#4177=VERTEX_POINT ( 'NONE', #6712 ) ;
#4184=CARTESIAN_POINT ( 'NONE',  ( -31.74999999999995737, 0.000000000000000000, 0.000000000000000000 ) ) ;
#4187=ORIENTED_EDGE ( 'NONE', *, *, #669, .T. ) ;
#4188=ORIENTED_EDGE ( 'NONE', *, *, #5105, .T. ) ;
#4190=DIRECTION ( 'NONE',  ( -0.7071067811865359154, 0.000000000000000000, 0.7071067811865591191 ) ) ;
#4213=ADVANCED_FACE ( 'NONE', ( #3481 ), #6618, .T. ) ;
#4220=CARTESIAN_POINT ( 'NONE',  ( 2.000000000000000000, 0.8865213383406717051, 1.535499999999998533 ) ) ;
#4225=AXIS2_PLACEMENT_3D ( 'NONE', #4719, #7955, #3605 ) ;
#4232=VECTOR ( 'NONE', #4190, 1000.000000000000000 ) ;
#4249=DIRECTION ( 'NONE',  ( -0.000000000000000000, 0.8660254037844391517, 0.4999999999999990563 ) ) ;
#4267=VERTEX_POINT ( 'NONE', #4944 ) ;
#4270=CARTESIAN_POINT ( 'NONE',  ( 24.00000000000000000, 0.000000000000000000, 0.000000000000000000 ) ) ;
#4272=CARTESIAN_POINT ( 'NONE',  ( -31.74999999999995737, 0.000000000000000000, 3.500000000000000000 ) ) ;
#4279=DIRECTION ( 'NONE',  ( -1.000000000000000000, -0.000000000000000000, -0.000000000000000000 ) ) ;
#4281=CARTESIAN_POINT ( 'NONE',  ( 2.000000000000000000, 1.773042676681340968, -2.276824562219559311E-15 ) ) ;
#4288=ORIENTED_EDGE ( 'NONE', *, *, #1722, .T. ) ;
#4290=DIRECTION ( 'NONE',  ( 1.000000000000000000, 0.000000000000000000, 0.000000000000000000 ) ) ;
#4295=ORIENTED_EDGE ( 'NONE', *, *, #174, .F. ) ;
#4296=ORIENTED_EDGE ( 'NONE', *, *, #1241, .T. ) ;
#4323=DIRECTION ( 'NONE',  ( 0.000000000000000000, 0.000000000000000000, -1.000000000000000000 ) ) ;
#4330=LINE ( 'NONE', #587, #4749 ) ;
#4338=CARTESIAN_POINT ( 'NONE',  ( 3.999999999999999112, 0.000000000000000000, 0.000000000000000000 ) ) ;
#4352=CARTESIAN_POINT ( 'NONE',  ( 2.000000000000000000, -1.773042676681340968, 2.059984127722458425E-15 ) ) ;
#4367=CIRCLE ( 'NONE', #1987, 3.299999999999999822 ) ;
#4373=ORIENTED_EDGE ( 'NONE', *, *, #7250, .T. ) ;
#4376=DIRECTION ( 'NONE',  ( 0.000000000000000000, 0.000000000000000000, -1.000000000000000000 ) ) ;
#4389=DIRECTION ( 'NONE',  ( -1.000000000000000000, -0.000000000000000000, -0.000000000000000000 ) ) ;
#4392=AXIS2_PLACEMENT_3D ( 'NONE', #3193, #641, #3858 ) ;
#4407=DIRECTION ( 'NONE',  ( -1.000000000000000000, -0.000000000000000000, -0.000000000000000000 ) ) ;
#4416=DIRECTION ( 'NONE',  ( 0.000000000000000000, 0.4999999999999990008, -0.8660254037844391517 ) ) ;
#4440=DIRECTION ( 'NONE',  ( -1.000000000000000000, -0.000000000000000000, -0.000000000000000000 ) ) ;
#4453=VERTEX_POINT ( 'NONE', #5194 ) ;
#4460=DIRECTION ( 'NONE',  ( 0.000000000000000000, 0.000000000000000000, 1.000000000000000000 ) ) ;
#4470=VECTOR ( 'NONE', #3397, 1000.000000000000000 ) ;
#4475=AXIS2_PLACEMENT_3D ( 'NONE', #4987, #3688, #3611 ) ;
#4487=AXIS2_PLACEMENT_3D ( 'NONE', #6383, #7042, #1269 ) ;
#4525=AXIS2_PLACEMENT_3D ( 'NONE', #7929, #172, #2254 ) ;
#4529=CIRCLE ( 'NONE', #4392, 1.535500000000000087 ) ;
#4532=FACE_OUTER_BOUND ( 'NONE', #5861, .T. ) ;
#4541=EDGE_LOOP ( 'NONE', ( #106, #6315, #2460, #3138, #7493 ) ) ;
#4570=VERTEX_POINT ( 'NONE', #2488 ) ;
#4582=DIRECTION ( 'NONE',  ( 0.000000000000000000, -1.000000000000000000, 9.783878858594330870E-16 ) ) ;
#4587=DIRECTION ( 'NONE',  ( -1.000000000000000000, -0.000000000000000000, -0.000000000000000000 ) ) ;
#4605=CARTESIAN_POINT ( 'NONE',  ( 0.1999999999999987899, 0.000000000000000000, 3.299999999999999822 ) ) ;
#4641=ORIENTED_EDGE ( 'NONE', *, *, #3147, .F. ) ;
#4643=AXIS2_PLACEMENT_3D ( 'NONE', #5754, #45, #2597 ) ;
#4655=AXIS2_PLACEMENT_3D ( 'NONE', #3637, #4975, #3099 ) ;
#4656=LINE ( 'NONE', #2704, #2368 ) ;
#4689=LINE ( 'NONE', #5322, #4470 ) ;
#4693=DIRECTION ( 'NONE',  ( 0.000000000000000000, 0.4999999999999990008, -0.8660254037844391517 ) ) ;
#4713=EDGE_CURVE ( 'NONE', #5731, #3952, #1514, .T. ) ;
#4719=CARTESIAN_POINT ( 'NONE',  ( 4.199999999999995737, 0.000000000000000000, -2.200000000000001066 ) ) ;
#4725=VECTOR ( 'NONE', #6547, 1000.000000000000227 ) ;
#4739=CARTESIAN_POINT ( 'NONE',  ( 0.000000000000000000, 0.000000000000000000, 3.299999999999999822 ) ) ;
#4749=VECTOR ( 'NONE', #6374, 1000.000000000000000 ) ;
#4778=DIRECTION ( 'NONE',  ( 0.000000000000000000, -0.4999999999999993339, 0.8660254037844389297 ) ) ;
#4780=ADVANCED_FACE ( 'NONE', ( #3545 ), #112, .F. ) ;
#4781=VECTOR ( 'NONE', #5464, 1000.000000000000227 ) ;
#4790=FACE_OUTER_BOUND ( 'NONE', #994, .T. ) ;
#4807=CARTESIAN_POINT ( 'NONE',  ( 4.199999999999995737, 0.000000000000000000, 0.000000000000000000 ) ) ;
#4812=ORIENTED_EDGE ( 'NONE', *, *, #6407, .F. ) ;
#4826=ORIENTED_EDGE ( 'NONE', *, *, #7470, .F. ) ;
#4833=( GEOMETRIC_REPRESENTATION_CONTEXT ( 3 ) GLOBAL_UNCERTAINTY_ASSIGNED_CONTEXT ( ( #2732 ) ) GLOBAL_UNIT_ASSIGNED_CONTEXT ( ( #7276, #6527, #4923 ) ) REPRESENTATION_CONTEXT ( 'NONE', 'WORKASPACE' ) );
#4839=PRODUCT ( 'socket head cap screw_iso_ISO 4762 M4 x 20 - 20N', 'socket head cap screw_iso_ISO 4762 M4 x 20 - 20N', '', ( #7225 ) ) ;
#4844=ORIENTED_EDGE ( 'NONE', *, *, #3459, .F. ) ;
#4845=LINE ( 'NONE', #4220, #491 ) ;
#4847=DIRECTION ( 'NONE',  ( 1.000000000000000000, 0.000000000000000000, 0.000000000000000000 ) ) ;
#4849=DIRECTION ( 'NONE',  ( -1.000000000000000000, -0.000000000000000000, -0.000000000000000000 ) ) ;
#4854=EDGE_LOOP ( 'NONE', ( #1670, #4826, #541, #8199, #4930 ) ) ;
#4859=DIRECTION ( 'NONE',  ( 0.000000000000000000, -1.000000000000000000, 1.467581828789149729E-15 ) ) ;
#4866=ORIENTED_EDGE ( 'NONE', *, *, #325, .F. ) ;
#4872=CARTESIAN_POINT ( 'NONE',  ( 0.000000000000000000, -0.8865213383406690406, 1.535500000000000975 ) ) ;
#4881=AXIS2_PLACEMENT_3D ( 'NONE', #4057, #4100, #7832 ) ;
#4892=DIRECTION ( 'NONE',  ( 0.000000000000000000, 1.000000000000000000, -1.467581828789149532E-15 ) ) ;
#4903=DIRECTION ( 'NONE',  ( -1.000000000000000000, -0.000000000000000000, -0.000000000000000000 ) ) ;
#4917=ORIENTED_EDGE ( 'NONE', *, *, #1924, .F. ) ;
#4923=( NAMED_UNIT ( * ) SI_UNIT ( $, .STERADIAN. ) SOLID_ANGLE_UNIT ( ) );
#4930=ORIENTED_EDGE ( 'NONE', *, *, #48, .T. ) ;
#4938=ADVANCED_FACE ( 'NONE', ( #3892 ), #2636, .T. ) ;
#4944=CARTESIAN_POINT ( 'NONE',  ( 2.000000000000000000, -0.8865213383406721492, -1.535499999999999199 ) ) ;
#4950=CARTESIAN_POINT ( 'NONE',  ( 2.000000000000000000, 0.000000000000000000, 0.000000000000000000 ) ) ;
#4953=CARTESIAN_POINT ( 'NONE',  ( 3.999999999999997335, 2.694222958124178486E-16, 2.200000000000001066 ) ) ;
#4972=DIRECTION ( 'NONE',  ( -1.000000000000000000, -0.000000000000000000, -0.000000000000000000 ) ) ;
#4975=DIRECTION ( 'NONE',  ( -1.000000000000000000, -0.000000000000000000, -0.000000000000000000 ) ) ;
#4982=CARTESIAN_POINT ( 'NONE',  ( 2.000000000000000000, 0.000000000000000000, 0.000000000000000000 ) ) ;
#4987=CARTESIAN_POINT ( 'NONE',  ( 4.199999999999995737, 0.000000000000000000, 0.000000000000000000 ) ) ;
#5006=ORIENTED_EDGE ( 'NONE', *, *, #100, .T. ) ;
#5048=EDGE_LOOP ( 'NONE', ( #4641, #15 ) ) ;
#5053=VECTOR ( 'NONE', #4587, 1000.000000000000000 ) ;
#5056=ORIENTED_EDGE ( 'NONE', *, *, #784, .F. ) ;
#5059=EDGE_CURVE ( 'NONE', #7189, #7486, #3983, .T. ) ;
#5071=AXIS2_PLACEMENT_3D ( 'NONE', #4270, #4440, #2400 ) ;
#5083=VERTEX_POINT ( 'NONE', #2713 ) ;
#5089=CARTESIAN_POINT ( 'NONE',  ( 2.000000000000000000, -0.8865213383406690406, 1.535500000000000975 ) ) ;
#5101=ORIENTED_EDGE ( 'NONE', *, *, #4168, .F. ) ;
#5105=EDGE_CURVE ( 'NONE', #5142, #821, #6649, .T. ) ;
#5125=DIRECTION ( 'NONE',  ( 0.000000000000000000, 0.8660254037844380415, -0.5000000000000012212 ) ) ;
#5128=FACE_OUTER_BOUND ( 'NONE', #1929, .T. ) ;
#5142=VERTEX_POINT ( 'NONE', #6524 ) ;
#5150=CARTESIAN_POINT ( 'NONE',  ( 2.000000000000000000, -1.329782007511004727, 0.7677500000000014868 ) ) ;
#5152=DIRECTION ( 'NONE',  ( 0.000000000000000000, 0.000000000000000000, 1.000000000000000000 ) ) ;
#5163=CIRCLE ( 'NONE', #7917, 1.535500000000000087 ) ;
#5164=ORIENTED_EDGE ( 'NONE', *, *, #6854, .F. ) ;
#5170=VECTOR ( 'NONE', #960, 1000.000000000000000 ) ;
#5171=ORIENTED_EDGE ( 'NONE', *, *, #5402, .T. ) ;
#5179=CIRCLE ( 'NONE', #2646, 1.535500000000000087 ) ;
#5180=EDGE_LOOP ( 'NONE', ( #6309, #3028, #5707, #4148 ) ) ;
#5184=DIRECTION ( 'NONE',  ( 0.000000000000000000, 0.5000000000000009992, 0.8660254037844381525 ) ) ;
#5185=ADVANCED_FACE ( 'NONE', ( #7355 ), #912, .T. ) ;
#5194=CARTESIAN_POINT ( 'NONE',  ( 4.000000000000003553, 4.286263797015736595E-16, -3.500000000000000000 ) ) ;
#5221=ADVANCED_FACE ( 'NONE', ( #4790 ), #1713, .T. ) ;
#5223=ORIENTED_EDGE ( 'NONE', *, *, #6504, .T. ) ;
#5276=FACE_OUTER_BOUND ( 'NONE', #2943, .T. ) ;
#5290=VECTOR ( 'NONE', #1794, 1000.000000000000227 ) ;
#5306=AXIS2_PLACEMENT_3D ( 'NONE', #455, #2916, #7395 ) ;
#5322=CARTESIAN_POINT ( 'NONE',  ( 2.000000000000000000, 1.880445160090761061E-16, -1.535500000000000087 ) ) ;
#5323=PRODUCT_DEFINITION_CONTEXT ( 'detailed design', #2796, 'design' ) ;
#5327=MECHANICAL_DESIGN_GEOMETRIC_PRESENTATION_REPRESENTATION('',(#2134),#5728);
#5349=ORIENTED_EDGE ( 'NONE', *, *, #6854, .T. ) ;
#5350=FACE_OUTER_BOUND ( 'NONE', #122, .T. ) ;
#5352=DIRECTION ( 'NONE',  ( -0.000000000000000000, 0.000000000000000000, 1.000000000000000000 ) ) ;
#5390=PLANE ( 'NONE',  #4881 ) ;
#5398=AXIS2_PLACEMENT_3D ( 'NONE', #3523, #3447, #312 ) ;
#5402=EDGE_CURVE ( 'NONE', #1419, #4570, #6371, .T. ) ;
#5404=DIRECTION ( 'NONE',  ( -1.000000000000000000, -0.000000000000000000, -0.000000000000000000 ) ) ;
#5431=DIRECTION ( 'NONE',  ( 0.000000000000000000, 0.000000000000000000, -1.000000000000000000 ) ) ;
#5437=DIRECTION ( 'NONE',  ( 1.000000000000000000, 0.000000000000000000, 0.000000000000000000 ) ) ;
#5439=LINE ( 'NONE', #6056, #694 ) ;
#5463=LINE ( 'NONE', #2917, #1202 ) ;
#5464=DIRECTION ( 'NONE',  ( 0.000000000000000000, -0.5000000000000008882, -0.8660254037844380415 ) ) ;
#5465=EDGE_LOOP ( 'NONE', ( #6436, #321, #5349, #6941, #6982 ) ) ;
#5466=ADVANCED_FACE ( 'NONE', ( #6517, #903 ), #6441, .T. ) ;
#5474=FACE_OUTER_BOUND ( 'NONE', #2130, .T. ) ;
#5502=FILL_AREA_STYLE_COLOUR ( '', #6678 ) ;
#5514=CARTESIAN_POINT ( 'NONE',  ( -31.74999999999995737, 4.286263797015736595E-16, -3.500000000000000000 ) ) ;
#5516=ORIENTED_EDGE ( 'NONE', *, *, #291, .T. ) ;
#5529=FACE_OUTER_BOUND ( 'NONE', #4541, .T. ) ;
#5545=ORIENTED_EDGE ( 'NONE', *, *, #3347, .F. ) ;
#5560=CIRCLE ( 'NONE', #6477, 1.610000000000000098 ) ;
#5598=ADVANCED_FACE ( 'NONE', ( #1077 ), #448, .F. ) ;
#5599=CARTESIAN_POINT ( 'NONE',  ( -31.74999999999995737, 0.000000000000000000, 0.000000000000000000 ) ) ;
#5622=ORIENTED_EDGE ( 'NONE', *, *, #2494, .T. ) ;
#5627=DIRECTION ( 'NONE',  ( 0.000000000000000000, 0.000000000000000000, -1.000000000000000000 ) ) ;
#5639=DIRECTION ( 'NONE',  ( 0.000000000000000000, -9.783878858594330870E-16, -1.000000000000000000 ) ) ;
#5643=EDGE_LOOP ( 'NONE', ( #4373, #5719 ) ) ;
#5652=EDGE_LOOP ( 'NONE', ( #1459, #3964, #1699 ) ) ;
#5670=EDGE_LOOP ( 'NONE', ( #2954, #4866, #5164 ) ) ;
#5702=EDGE_CURVE ( 'NONE', #1678, #135, #538, .T. ) ;
#5707=ORIENTED_EDGE ( 'NONE', *, *, #7250, .F. ) ;
#5719=ORIENTED_EDGE ( 'NONE', *, *, #1117, .T. ) ;
#5728=( GEOMETRIC_REPRESENTATION_CONTEXT ( 3 ) GLOBAL_UNCERTAINTY_ASSIGNED_CONTEXT ( ( #2881 ) ) GLOBAL_UNIT_ASSIGNED_CONTEXT ( ( #1183, #1816, #3600 ) ) REPRESENTATION_CONTEXT ( 'NONE', 'WORKASPACE' ) );
#5731=VERTEX_POINT ( 'NONE', #6358 ) ;
#5738=EDGE_LOOP ( 'NONE', ( #5056, #5516, #2143 ) ) ;
#5739=DIRECTION ( 'NONE',  ( 0.000000000000000000, 0.000000000000000000, 1.000000000000000000 ) ) ;
#5752=EDGE_LOOP ( 'NONE', ( #4844, #6486, #4, #2055, #7022 ) ) ;
#5754=CARTESIAN_POINT ( 'NONE',  ( 2.000000000000000000, 1.773042676681340968, -2.276824562219559311E-15 ) ) ;
#5822=CARTESIAN_POINT ( 'NONE',  ( 3.999999999999999112, 3.500000000000000000, 0.000000000000000000 ) ) ;
#5852=VERTEX_POINT ( 'NONE', #2041 ) ;
#5861=EDGE_LOOP ( 'NONE', ( #5223, #4063, #2691, #3137, #4188 ) ) ;
#5864=VERTEX_POINT ( 'NONE', #2008 ) ;
#5882=DIRECTION ( 'NONE',  ( 0.000000000000000000, 0.000000000000000000, -1.000000000000000000 ) ) ;
#5889=( GEOMETRIC_REPRESENTATION_CONTEXT ( 3 ) GLOBAL_UNCERTAINTY_ASSIGNED_CONTEXT ( ( #1496 ) ) GLOBAL_UNIT_ASSIGNED_CONTEXT ( ( #1674, #416, #1129 ) ) REPRESENTATION_CONTEXT ( 'NONE', 'WORKASPACE' ) );
#5911=CARTESIAN_POINT ( 'NONE',  ( 2.000000000000000000, 1.329782007511004727, -0.7677500000000019309 ) ) ;
#5929=CARTESIAN_POINT ( 'NONE',  ( 2.000000000000000000, -0.8865213383406690406, 1.535500000000000975 ) ) ;
#5932=CIRCLE ( 'NONE', #4487, 3.500000000000000000 ) ;
#5947=CLOSED_SHELL ( 'NONE', ( #4780, #6863, #7593, #438, #2276, #2365, #6785, #1675, #5466, #6478, #4213, #2413, #1953, #5185, #2780, #5598, #4938, #5221, #3263, #6645, #8027, #7588, #4004, #6707, #7761, #594, #7299 ) ) ;
#5957=CARTESIAN_POINT ( 'NONE',  ( 0.000000000000000000, 0.8865213383406685965, -1.535500000000000753 ) ) ;
#5958=AXIS2_PLACEMENT_3D ( 'NONE', #7907, #5437, #890 ) ;
#5963=FACE_BOUND ( 'NONE', #7100, .T. ) ;
#5984=ORIENTED_EDGE ( 'NONE', *, *, #3166, .F. ) ;
#5985=CARTESIAN_POINT ( 'NONE',  ( 0.1999999999999987899, 0.000000000000000000, 0.000000000000000000 ) ) ;
#6005=CARTESIAN_POINT ( 'NONE',  ( 24.00000000000000000, 0.000000000000000000, 0.000000000000000000 ) ) ;
#6010=LINE ( 'NONE', #5929, #4725 ) ;
#6019=PRODUCT_DEFINITION_FORMATION_WITH_SPECIFIED_SOURCE ( 'ANY', '', #4839, .NOT_KNOWN. ) ;
#6031=EDGE_CURVE ( 'NONE', #3952, #6185, #7399, .T. ) ;
#6050=TOROIDAL_SURFACE ( 'NONE', #4475, 2.200000000000001066, 0.2000000000000000111 ) ;
#6056=CARTESIAN_POINT ( 'NONE',  ( 0.000000000000000000, 1.773042676681340968, -2.276824562219559311E-15 ) ) ;
#6066=CARTESIAN_POINT ( 'NONE',  ( 0.1999999999999987899, 0.000000000000000000, 3.500000000000000000 ) ) ;
#6084=EDGE_CURVE ( 'NONE', #1617, #3952, #1708, .T. ) ;
#6101=CIRCLE ( 'NONE', #5958, 2.000000000000000888 ) ;
#6131=ORIENTED_EDGE ( 'NONE', *, *, #6504, .F. ) ;
#6132=FACE_OUTER_BOUND ( 'NONE', #65, .T. ) ;
#6140=DIRECTION ( 'NONE',  ( 0.000000000000000000, 0.000000000000000000, 1.000000000000000000 ) ) ;
#6147=ORIENTED_EDGE ( 'NONE', *, *, #174, .T. ) ;
#6158=AXIS2_PLACEMENT_3D ( 'NONE', #1408, #731, #5739 ) ;
#6169=CARTESIAN_POINT ( 'NONE',  ( 3.999999999999997335, 0.000000000000000000, -2.200000000000001066 ) ) ;
#6170=DIRECTION ( 'NONE',  ( 0.000000000000000000, -1.000000000000000000, 9.783878858594330870E-16 ) ) ;
#6182=AXIS2_PLACEMENT_3D ( 'NONE', #7997, #2856, #6583 ) ;
#6185=VERTEX_POINT ( 'NONE', #6169 ) ;
#6211=CARTESIAN_POINT ( 'NONE',  ( 0.1999999999999987899, 0.000000000000000000, 0.000000000000000000 ) ) ;
#6236=ORIENTED_EDGE ( 'NONE', *, *, #7470, .T. ) ;
#6238=ORIENTED_EDGE ( 'NONE', *, *, #3860, .T. ) ;
#6250=CARTESIAN_POINT ( 'NONE',  ( 2.000000000000000000, 0.000000000000000000, 0.000000000000000000 ) ) ;
#6262=LINE ( 'NONE', #606, #1045 ) ;
#6271=LINE ( 'NONE', #1921, #1857 ) ;
#6309=ORIENTED_EDGE ( 'NONE', *, *, #6084, .F. ) ;
#6315=ORIENTED_EDGE ( 'NONE', *, *, #5105, .F. ) ;
#6338=VECTOR ( 'NONE', #6450, 1000.000000000000000 ) ;
#6344=CARTESIAN_POINT ( 'NONE',  ( 2.000000000000000000, 0.8865213383406685965, -1.535500000000000753 ) ) ;
#6351=VECTOR ( 'NONE', #4582, 1000.000000000000000 ) ;
#6358=CARTESIAN_POINT ( 'NONE',  ( 23.61000000000001364, 2.449293598294707400E-16, -2.000000000000000444 ) ) ;
#6363=AXIS2_PLACEMENT_3D ( 'NONE', #3908, #5125, #2723 ) ;
#6371=LINE ( 'NONE', #2628, #7681 ) ;
#6372=PLANE ( 'NONE',  #4643 ) ;
#6374=DIRECTION ( 'NONE',  ( 0.000000000000000000, -1.000000000000000000, 9.783878858594330870E-16 ) ) ;
#6383=CARTESIAN_POINT ( 'NONE',  ( 0.1999999999999987899, 0.000000000000000000, 0.000000000000000000 ) ) ;
#6393=EDGE_CURVE ( 'NONE', #4453, #5852, #770, .T. ) ;
#6394=EDGE_CURVE ( 'NONE', #5083, #4177, #3527, .T. ) ;
#6407=EDGE_CURVE ( 'NONE', #3462, #531, #4367, .T. ) ;
#6408=EDGE_CURVE ( 'NONE', #4177, #5731, #1176, .T. ) ;
#6418=CARTESIAN_POINT ( 'NONE',  ( 2.000000000000000000, -0.8865213383406690406, 1.535500000000000975 ) ) ;
#6420=CARTESIAN_POINT ( 'NONE',  ( 4.000000000000003553, 0.000000000000000000, 0.000000000000000000 ) ) ;
#6436=ORIENTED_EDGE ( 'NONE', *, *, #1722, .F. ) ;
#6441=PLANE ( 'NONE',  #7015 ) ;
#6450=DIRECTION ( 'NONE',  ( 0.000000000000000000, 1.000000000000000000, -1.467581828789149532E-15 ) ) ;
#6454=DIRECTION ( 'NONE',  ( 1.000000000000000000, 0.000000000000000000, 0.000000000000000000 ) ) ;
#6462=CIRCLE ( 'NONE', #3685, 3.500000000000000000 ) ;
#6477=AXIS2_PLACEMENT_3D ( 'NONE', #6948, #3802, #4460 ) ;
#6478=ADVANCED_FACE ( 'NONE', ( #2982 ), #8041, .T. ) ;
#6480=EDGE_CURVE ( 'NONE', #5864, #5731, #6271, .T. ) ;
#6482=CIRCLE ( 'NONE', #5071, 1.610000000000000098 ) ;
#6486=ORIENTED_EDGE ( 'NONE', *, *, #5702, .F. ) ;
#6488=AXIS2_PLACEMENT_3D ( 'NONE', #6418, #3230, #5184 ) ;
#6504=EDGE_CURVE ( 'NONE', #821, #1158, #1831, .T. ) ;
#6517=FACE_BOUND ( 'NONE', #5643, .T. ) ;
#6524=CARTESIAN_POINT ( 'NONE',  ( 2.000000000000000000, 1.773042676681340968, -2.276824562219559311E-15 ) ) ;
#6527=( NAMED_UNIT ( * ) PLANE_ANGLE_UNIT ( ) SI_UNIT ( $, .RADIAN. ) );
#6541=PLANE ( 'NONE',  #6363 ) ;
#6547=DIRECTION ( 'NONE',  ( 0.000000000000000000, -0.5000000000000008882, -0.8660254037844380415 ) ) ;
#6562=CARTESIAN_POINT ( 'NONE',  ( 0.000000000000000000, -0.8865213383406690406, 1.535500000000000975 ) ) ;
#6566=CIRCLE ( 'NONE', #6182, 1.535500000000000087 ) ;
#6568=CARTESIAN_POINT ( 'NONE',  ( 3.999999999999999112, 0.000000000000000000, 0.000000000000000000 ) ) ;
#6581=CARTESIAN_POINT ( 'NONE',  ( 24.00000000000000000, 1.610000000000000098, 0.000000000000000000 ) ) ;
#6583=DIRECTION ( 'NONE',  ( 0.000000000000000000, 0.000000000000000000, 1.000000000000000000 ) ) ;
#6618=CONICAL_SURFACE ( 'NONE', #526, 1.610000000000000098, 0.7853981633974647103 ) ;
#6645=ADVANCED_FACE ( 'NONE', ( #4532 ), #6541, .F. ) ;
#6649=LINE ( 'NONE', #2091, #5053 ) ;
#6655=ORIENTED_EDGE ( 'NONE', *, *, #100, .F. ) ;
#6665=ORIENTED_EDGE ( 'NONE', *, *, #6820, .F. ) ;
#6666=DIRECTION ( 'NONE',  ( 1.000000000000000000, 0.000000000000000000, 0.000000000000000000 ) ) ;
#6667=DIRECTION ( 'NONE',  ( -1.000000000000000000, -0.000000000000000000, -0.000000000000000000 ) ) ;
#6673=DIRECTION ( 'NONE',  ( 0.000000000000000000, 0.000000000000000000, 1.000000000000000000 ) ) ;
#6678=COLOUR_RGB ( '', 0.09019608, 0.27058824, 0.51372549) ;
#6687=ORIENTED_EDGE ( 'NONE', *, *, #2840, .F. ) ;
#6707=ADVANCED_FACE ( 'NONE', ( #390 ), #5390, .F. ) ;
#6708=FACE_OUTER_BOUND ( 'NONE', #2550, .T. ) ;
#6712=CARTESIAN_POINT ( 'NONE',  ( 23.61000000000001364, 0.000000000000000000, 2.000000000000000444 ) ) ;
#6750=ORIENTED_EDGE ( 'NONE', *, *, #7367, .T. ) ;
#6758=DIRECTION ( 'NONE',  ( 0.000000000000000000, -0.4999999999999993339, 0.8660254037844389297 ) ) ;
#6785=ADVANCED_FACE ( 'NONE', ( #5963, #6708 ), #1014, .T. ) ;
#6788=SURFACE_STYLE_USAGE ( .BOTH. , #3547 ) ;
#6806=DIRECTION ( 'NONE',  ( 0.000000000000000000, 0.4999999999999993339, -0.8660254037844390407 ) ) ;
#6820=EDGE_CURVE ( 'NONE', #6988, #7449, #4845, .T. ) ;
#6833=DIRECTION ( 'NONE',  ( 0.000000000000000000, 0.000000000000000000, 1.000000000000000000 ) ) ;
#6853=VERTEX_POINT ( 'NONE', #1062 ) ;
#6854=EDGE_CURVE ( 'NONE', #1738, #2405, #5163, .T. ) ;
#6860=EDGE_LOOP ( 'NONE', ( #3654, #5101, #7314, #3486 ) ) ;
#6863=ADVANCED_FACE ( 'NONE', ( #6132 ), #8050, .T. ) ;
#6878=DIRECTION ( 'NONE',  ( -1.000000000000000000, -0.000000000000000000, -0.000000000000000000 ) ) ;
#6881=VECTOR ( 'NONE', #2872, 1000.000000000000000 ) ;
#6884=DIRECTION ( 'NONE',  ( 0.000000000000000000, 1.000000000000000000, -1.224646799147353207E-16 ) ) ;
#6888=AXIS2_PLACEMENT_3D ( 'NONE', #5985, #4124, #7190 ) ;
#6889=DIRECTION ( 'NONE',  ( 0.000000000000000000, 0.000000000000000000, 1.000000000000000000 ) ) ;
#6924=VERTEX_POINT ( 'NONE', #2099 ) ;
#6941=ORIENTED_EDGE ( 'NONE', *, *, #197, .T. ) ;
#6948=CARTESIAN_POINT ( 'NONE',  ( 24.00000000000000000, 0.000000000000000000, 0.000000000000000000 ) ) ;
#6958=DIRECTION ( 'NONE',  ( -1.000000000000000000, -0.000000000000000000, -0.000000000000000000 ) ) ;
#6962=CARTESIAN_POINT ( 'NONE',  ( 2.000000000000000000, 0.8865213383406717051, 1.535499999999998533 ) ) ;
#6982=ORIENTED_EDGE ( 'NONE', *, *, #386, .T. ) ;
#6985=DIRECTION ( 'NONE',  ( -0.5000000000000061062, 0.000000000000000000, 0.8660254037844351549 ) ) ;
#6988=VERTEX_POINT ( 'NONE', #6962 ) ;
#7013=DIRECTION ( 'NONE',  ( 0.000000000000000000, -1.000000000000000000, 0.000000000000000000 ) ) ;
#7015=AXIS2_PLACEMENT_3D ( 'NONE', #5822, #3338, #2705 ) ;
#7022=ORIENTED_EDGE ( 'NONE', *, *, #1924, .T. ) ;
#7038=VERTEX_POINT ( 'NONE', #5150 ) ;
#7042=DIRECTION ( 'NONE',  ( 1.000000000000000000, 0.000000000000000000, 0.000000000000000000 ) ) ;
#7091=ORIENTED_EDGE ( 'NONE', *, *, #8017, .F. ) ;
#7100=EDGE_LOOP ( 'NONE', ( #5622, #5545, #2667, #5006, #7529, #6131 ) ) ;
#7118=VECTOR ( 'NONE', #2582, 1000.000000000000000 ) ;
#7129=DIRECTION ( 'NONE',  ( 0.000000000000000000, 0.000000000000000000, -1.000000000000000000 ) ) ;
#7161=AXIS2_PLACEMENT_3D ( 'NONE', #1040, #7445, #5627 ) ;
#7188=EDGE_LOOP ( 'NONE', ( #3554, #1299, #7971, #1758 ) ) ;
#7189=VERTEX_POINT ( 'NONE', #3424 ) ;
#7190=DIRECTION ( 'NONE',  ( 0.000000000000000000, 0.000000000000000000, 1.000000000000000000 ) ) ;
#7216=CARTESIAN_POINT ( 'NONE',  ( 2.000000000000000000, 2.253471898105738645E-15, 1.535499999999999865 ) ) ;
#7225=PRODUCT_CONTEXT ( 'NONE', #2367, 'mechanical' ) ;
#7243=CARTESIAN_POINT ( 'NONE',  ( 24.00000000000000000, 0.000000000000000000, 0.000000000000000000 ) ) ;
#7250=EDGE_CURVE ( 'NONE', #6185, #2702, #1460, .T. ) ;
#7257=LINE ( 'NONE', #1499, #4096 ) ;
#7258=CARTESIAN_POINT ( 'NONE',  ( 4.000000000000003553, 0.000000000000000000, 0.000000000000000000 ) ) ;
#7263=SHAPE_DEFINITION_REPRESENTATION ( #3585, #7870 ) ;
#7276=( LENGTH_UNIT ( ) NAMED_UNIT ( * ) SI_UNIT ( .MILLI., .METRE. ) );
#7283=VECTOR ( 'NONE', #4416, 1000.000000000000227 ) ;
#7295=DIRECTION ( 'NONE',  ( -1.000000000000000000, 0.000000000000000000, -0.000000000000000000 ) ) ;
#7299=ADVANCED_FACE ( 'NONE', ( #3893 ), #3195, .F. ) ;
#7302=CARTESIAN_POINT ( 'NONE',  ( 2.000000000000000000, 1.329782007511006281, 0.7677499999999990443 ) ) ;
#7314=ORIENTED_EDGE ( 'NONE', *, *, #6031, .T. ) ;
#7334=DIRECTION ( 'NONE',  ( 0.000000000000000000, 0.000000000000000000, -1.000000000000000000 ) ) ;
#7337=PLANE ( 'NONE',  #2419 ) ;
#7338=EDGE_LOOP ( 'NONE', ( #5171, #6238, #7473 ) ) ;
#7353=ORIENTED_EDGE ( 'NONE', *, *, #4168, .T. ) ;
#7355=FACE_OUTER_BOUND ( 'NONE', #704, .T. ) ;
#7364=SURFACE_STYLE_FILL_AREA ( #560 ) ;
#7367=EDGE_CURVE ( 'NONE', #7189, #531, #7952, .T. ) ;
#7374=DIRECTION ( 'NONE',  ( 0.000000000000000000, 0.000000000000000000, 1.000000000000000000 ) ) ;
#7387=CARTESIAN_POINT ( 'NONE',  ( 2.000000000000000000, -1.329782007511006281, -0.7677499999999984892 ) ) ;
#7395=DIRECTION ( 'NONE',  ( 0.000000000000000000, 0.000000000000000000, 1.000000000000000000 ) ) ;
#7399=CIRCLE ( 'NONE', #4225, 0.2000000000000000944 ) ;
#7424=LINE ( 'NONE', #4272, #124 ) ;
#7429=ORIENTED_EDGE ( 'NONE', *, *, #6480, .T. ) ;
#7431=CARTESIAN_POINT ( 'NONE',  ( 24.00000000000000000, 0.000000000000000000, 1.610000000000000098 ) ) ;
#7433=DIRECTION ( 'NONE',  ( 0.000000000000000000, -0.8660254037844390407, -0.4999999999999993339 ) ) ;
#7445=DIRECTION ( 'NONE',  ( 1.000000000000000000, 0.000000000000000000, 0.000000000000000000 ) ) ;
#7448=SHAPE_REPRESENTATION_RELATIONSHIP ( 'NONE' , 'NONE' ,  #7870, #7647 ) ;
#7449=VERTEX_POINT ( 'NONE', #4164 ) ;
#7470=EDGE_CURVE ( 'NONE', #4267, #6924, #5463, .T. ) ;
#7473=ORIENTED_EDGE ( 'NONE', *, *, #386, .F. ) ;
#7480=PLANE ( 'NONE',  #7540 ) ;
#7485=VERTEX_POINT ( 'NONE', #2991 ) ;
#7486=VERTEX_POINT ( 'NONE', #6066 ) ;
#7490=STYLED_ITEM ( 'NONE', ( #498 ), #7647 ) ;
#7493=ORIENTED_EDGE ( 'NONE', *, *, #6820, .T. ) ;
#7494=VECTOR ( 'NONE', #3208, 1000.000000000000114 ) ;
#7529=ORIENTED_EDGE ( 'NONE', *, *, #3650, .F. ) ;
#7531=ORIENTED_EDGE ( 'NONE', *, *, #7367, .F. ) ;
#7540=AXIS2_PLACEMENT_3D ( 'NONE', #7609, #3660, #4323 ) ;
#7552=VECTOR ( 'NONE', #3830, 1000.000000000000114 ) ;
#7588=ADVANCED_FACE ( 'NONE', ( #547 ), #2296, .F. ) ;
#7590=CARTESIAN_POINT ( 'NONE',  ( 2.000000000000000000, 0.000000000000000000, 0.000000000000000000 ) ) ;
#7593=ADVANCED_FACE ( 'NONE', ( #2331 ), #1878, .F. ) ;
#7599=DIRECTION ( 'NONE',  ( 0.000000000000000000, 0.000000000000000000, -1.000000000000000000 ) ) ;
#7609=CARTESIAN_POINT ( 'NONE',  ( 2.000000000000000000, 1.773042676681340968, -2.276824562219559311E-15 ) ) ;
#7621=ORIENTED_EDGE ( 'NONE', *, *, #2929, .F. ) ;
#7647=ADVANCED_BREP_SHAPE_REPRESENTATION ( '', ( #1247, #1587 ), #4833 ) ;
#7665=PRODUCT_DEFINITION ( 'UNKNOWN', '', #6019, #5323 ) ;
#7681=VECTOR ( 'NONE', #3711, 1000.000000000000114 ) ;
#7718=CARTESIAN_POINT ( 'NONE',  ( 2.000000000000000000, 1.773042676681340968, -2.276824562219559311E-15 ) ) ;
#7725=ORIENTED_EDGE ( 'NONE', *, *, #6480, .F. ) ;
#7734=LINE ( 'NONE', #2707, #6351 ) ;
#7755=EDGE_CURVE ( 'NONE', #7485, #1738, #711, .T. ) ;
#7761=ADVANCED_FACE ( 'NONE', ( #1301 ), #6372, .F. ) ;
#7774=AXIS2_PLACEMENT_3D ( 'NONE', #4605, #7013, #7129 ) ;
#7777=DIRECTION ( 'NONE',  ( -1.000000000000000000, -0.000000000000000000, -0.000000000000000000 ) ) ;
#7786=CARTESIAN_POINT ( 'NONE',  ( -31.74999999999995737, 0.000000000000000000, 2.000000000000000888 ) ) ;
#7791=CARTESIAN_POINT ( 'NONE',  ( 4.199999999999995737, 0.000000000000000000, 2.000000000000000888 ) ) ;
#7805=AXIS2_PLACEMENT_3D ( 'NONE', #7258, #1578, #4114 ) ;
#7832=DIRECTION ( 'NONE',  ( 0.000000000000000000, 0.000000000000000000, -1.000000000000000000 ) ) ;
#7870=SHAPE_REPRESENTATION ( 'socket head cap screw_iso_ISO 4762 M4 x 20 - 20N', ( #1587 ), #4833 ) ;
#7876=ORIENTED_EDGE ( 'NONE', *, *, #687, .T. ) ;
#7902=CARTESIAN_POINT ( 'NONE',  ( 0.000000000000000000, 4.163799117101000559E-16, -3.299999999999999822 ) ) ;
#7907=CARTESIAN_POINT ( 'NONE',  ( 4.199999999999995737, 0.000000000000000000, 0.000000000000000000 ) ) ;
#7912=ORIENTED_EDGE ( 'NONE', *, *, #7755, .F. ) ;
#7917=AXIS2_PLACEMENT_3D ( 'NONE', #4982, #6878, #520 ) ;
#7929=CARTESIAN_POINT ( 'NONE',  ( 0.1999999999999987899, 4.041334437186265510E-16, -3.299999999999999822 ) ) ;
#7939=VECTOR ( 'NONE', #672, 1000.000000000000227 ) ;
#7951=PLANE ( 'NONE',  #843 ) ;
#7952=CIRCLE ( 'NONE', #4525, 0.2000000000000000944 ) ;
#7955=DIRECTION ( 'NONE',  ( 0.000000000000000000, -1.000000000000000000, 0.000000000000000000 ) ) ;
#7963=ORIENTED_EDGE ( 'NONE', *, *, #3147, .T. ) ;
#7971=ORIENTED_EDGE ( 'NONE', *, *, #904, .T. ) ;
#7997=CARTESIAN_POINT ( 'NONE',  ( 2.000000000000000000, 0.000000000000000000, 0.000000000000000000 ) ) ;
#8002=CARTESIAN_POINT ( 'NONE',  ( 23.61000000000001364, 0.000000000000000000, 0.000000000000000000 ) ) ;
#8014=CARTESIAN_POINT ( 'NONE',  ( 2.000000000000000000, -1.773042676681340968, 2.059984127722458425E-15 ) ) ;
#8016=LINE ( 'NONE', #327, #6881 ) ;
#8017=EDGE_CURVE ( 'NONE', #5864, #5083, #6482, .T. ) ;
#8027=ADVANCED_FACE ( 'NONE', ( #523 ), #1195, .F. ) ;
#8041=CYLINDRICAL_SURFACE ( 'NONE', #898, 2.000000000000000888 ) ;
#8043=PLANE ( 'NONE',  #3348 ) ;
#8045=CARTESIAN_POINT ( 'NONE',  ( 4.199999999999995737, 2.449293598294707893E-16, -2.000000000000000888 ) ) ;
#8050=TOROIDAL_SURFACE ( 'NONE', #2885, 3.299999999999999822, 0.2000000000000000111 ) ;
#8068=DIRECTION ( 'NONE',  ( 0.000000000000000000, 0.000000000000000000, -1.000000000000000000 ) ) ;
#8069=EDGE_CURVE ( 'NONE', #1738, #6988, #6262, .T. ) ;
#8079=EDGE_CURVE ( 'NONE', #3458, #4267, #8126, .T. ) ;
#8097=CARTESIAN_POINT ( 'NONE',  ( 2.000000000000000000, -0.8865213383406690406, 1.535500000000000975 ) ) ;
#8126=LINE ( 'NONE', #6344, #2773 ) ;
#8149=CIRCLE ( 'NONE', #6158, 1.535500000000000087 ) ;
#8153=DIRECTION ( 'NONE',  ( 0.000000000000000000, 1.000000000000000000, -9.783878858594330870E-16 ) ) ;
#8199=ORIENTED_EDGE ( 'NONE', *, *, #3860, .F. ) ;
#8203=DIRECTION ( 'NONE',  ( 1.000000000000000000, 0.000000000000000000, 0.000000000000000000 ) ) ;
ENDSEC;
END-ISO-10303-21;
